ISO-10303-21;
HEADER;
/* Generated by software containing ST-Developer
 * from STEP Tools, Inc. (www.steptools.com) 
 */

FILE_DESCRIPTION(
/* description */ ('Bin tilter linkage'),
/* implementation_level */ '2;1');

FILE_NAME(
/* name */ 'M4 short cap screw (9).step',
/* time_stamp */ '2026-10-28T03:26:24-07:00',
/* author */ (''),
/* organization */ (''),
/* preprocessor_version */ 'ST-DEVELOPER v20.2',
/* originating_system */ 'Autodesk Translation Framework v15.17.0.0',
/* authorisation */ '');

FILE_SCHEMA (('AUTOMOTIVE_DESIGN { 1 0 10303 214 3 1 1 }'));
ENDSEC;

DATA;
#10=MECHANICAL_DESIGN_GEOMETRIC_PRESENTATION_REPRESENTATION('',(#905),#23728);
#693=SHAPE_REPRESENTATION_RELATIONSHIP('SRR','None',#24158,#799);
#799=ADVANCED_BREP_SHAPE_REPRESENTATION('',(#1018),#23658);
#905=STYLED_ITEM('',(#24772),#1018);
#1018=MANIFOLD_SOLID_BREP('Body1',#12436);
#1293=FACE_BOUND('',#3208,.T.);
#1654=PLANE('',#14397);
#1655=PLANE('',#14402);
#1656=PLANE('',#14405);
#2224=FACE_OUTER_BOUND('',#3207,.T.);
#2225=FACE_OUTER_BOUND('',#3209,.T.);
#2226=FACE_OUTER_BOUND('',#3210,.T.);
#2227=FACE_OUTER_BOUND('',#3211,.T.);
#2228=FACE_OUTER_BOUND('',#3212,.T.);
#3207=EDGE_LOOP('',(#9673));
#3208=EDGE_LOOP('',(#9674));
#3209=EDGE_LOOP('',(#9675,#9676,#9677,#9678));
#3210=EDGE_LOOP('',(#9679));
#3211=EDGE_LOOP('',(#9680,#9681,#9682,#9683));
#3212=EDGE_LOOP('',(#9684));
#4159=LINE('',#21215,#4834);
#4160=LINE('',#21221,#4835);
#4834=VECTOR('',#17234,0.35);
#4835=VECTOR('',#17243,0.199999999999999);
#5539=CIRCLE('',#14398,0.35);
#5540=CIRCLE('',#14399,0.199999999999999);
#5541=CIRCLE('',#14401,0.35);
#5542=CIRCLE('',#14404,0.199999999999999);
#6389=VERTEX_POINT('',#21209);
#6390=VERTEX_POINT('',#21211);
#6391=VERTEX_POINT('',#21214);
#6392=VERTEX_POINT('',#21219);
#7576=EDGE_CURVE('',#6389,#6389,#5539,.T.);
#7577=EDGE_CURVE('',#6390,#6390,#5540,.T.);
#7578=EDGE_CURVE('',#6389,#6391,#4159,.T.);
#7579=EDGE_CURVE('',#6391,#6391,#5541,.T.);
#7580=EDGE_CURVE('',#6392,#6392,#5542,.T.);
#7581=EDGE_CURVE('',#6392,#6390,#4160,.T.);
#9673=ORIENTED_EDGE('',*,*,#7576,.T.);
#9674=ORIENTED_EDGE('',*,*,#7577,.F.);
#9675=ORIENTED_EDGE('',*,*,#7576,.F.);
#9676=ORIENTED_EDGE('',*,*,#7578,.T.);
#9677=ORIENTED_EDGE('',*,*,#7579,.T.);
#9678=ORIENTED_EDGE('',*,*,#7578,.F.);
#9679=ORIENTED_EDGE('',*,*,#7579,.F.);
#9680=ORIENTED_EDGE('',*,*,#7580,.F.);
#9681=ORIENTED_EDGE('',*,*,#7581,.T.);
#9682=ORIENTED_EDGE('',*,*,#7577,.T.);
#9683=ORIENTED_EDGE('',*,*,#7581,.F.);
#9684=ORIENTED_EDGE('',*,*,#7580,.T.);
#11435=CYLINDRICAL_SURFACE('',#14400,0.35);
#11436=CYLINDRICAL_SURFACE('',#14403,0.199999999999999);
#11949=ADVANCED_FACE('',(#2224,#1293),#1654,.T.);
#11950=ADVANCED_FACE('',(#2225),#11435,.T.);
#11951=ADVANCED_FACE('',(#2226),#1655,.F.);
#11952=ADVANCED_FACE('',(#2227),#11436,.T.);
#11953=ADVANCED_FACE('',(#2228),#1656,.T.);
#12436=CLOSED_SHELL('',(#11949,#11950,#11951,#11952,#11953));
#14396=AXIS2_PLACEMENT_3D('',#21207,#17224,#17225);
#14397=AXIS2_PLACEMENT_3D('',#21208,#17226,#17227);
#14398=AXIS2_PLACEMENT_3D('',#21210,#17228,#17229);
#14399=AXIS2_PLACEMENT_3D('',#21212,#17230,#17231);
#14400=AXIS2_PLACEMENT_3D('',#21213,#17232,#17233);
#14401=AXIS2_PLACEMENT_3D('',#21216,#17235,#17236);
#14402=AXIS2_PLACEMENT_3D('',#21217,#17237,#17238);
#14403=AXIS2_PLACEMENT_3D('',#21218,#17239,#17240);
#14404=AXIS2_PLACEMENT_3D('',#21220,#17241,#17242);
#14405=AXIS2_PLACEMENT_3D('',#21222,#17244,#17245);
#17224=DIRECTION('axis',(0.,0.,1.));
#17225=DIRECTION('refdir',(1.,0.,0.));
#17226=DIRECTION('center_axis',(0.,1.,0.));
#17227=DIRECTION('ref_axis',(1.,0.,0.));
#17228=DIRECTION('center_axis',(0.,1.,0.));
#17229=DIRECTION('ref_axis',(1.,0.,0.));
#17230=DIRECTION('center_axis',(0.,1.,0.));
#17231=DIRECTION('ref_axis',(1.,0.,0.));
#17232=DIRECTION('center_axis',(0.,1.,0.));
#17233=DIRECTION('ref_axis',(1.,0.,0.));
#17234=DIRECTION('',(0.,-1.,0.));
#17235=DIRECTION('center_axis',(0.,1.,0.));
#17236=DIRECTION('ref_axis',(1.,0.,0.));
#17237=DIRECTION('center_axis',(0.,1.,0.));
#17238=DIRECTION('ref_axis',(1.,0.,0.));
#17239=DIRECTION('center_axis',(0.,1.,0.));
#17240=DIRECTION('ref_axis',(1.,0.,0.));
#17241=DIRECTION('center_axis',(0.,1.,0.));
#17242=DIRECTION('ref_axis',(1.,0.,0.));
#17243=DIRECTION('',(0.,-1.,0.));
#17244=DIRECTION('center_axis',(0.,1.,0.));
#17245=DIRECTION('ref_axis',(1.,0.,0.));
#21207=CARTESIAN_POINT('',(0.,0.,0.));
#21208=CARTESIAN_POINT('Origin',(8.08877866266397,-0.8,19.7283489784518));
#21209=CARTESIAN_POINT('',(7.73877866266397,-0.8,19.7283489784518));
#21210=CARTESIAN_POINT('Origin',(8.08877866266397,-0.8,19.7283489784518));
#21211=CARTESIAN_POINT('',(7.88877866266397,-0.8,19.7283489784518));
#21212=CARTESIAN_POINT('Origin',(8.08877866266397,-0.8,19.7283489784518));
#21213=CARTESIAN_POINT('Origin',(8.08877866266397,-1.2,19.7283489784518));
#21214=CARTESIAN_POINT('',(7.73877866266397,-1.2,19.7283489784518));
#21215=CARTESIAN_POINT('',(7.73877866266397,-1.2,19.7283489784518));
#21216=CARTESIAN_POINT('Origin',(8.08877866266397,-1.2,19.7283489784518));
#21217=CARTESIAN_POINT('Origin',(8.08877866266397,-1.2,19.7283489784518));
#21218=CARTESIAN_POINT('Origin',(8.08877866266397,-0.8,19.7283489784518));
#21219=CARTESIAN_POINT('',(7.88877866266397,-0.1,19.7283489784518));
#21220=CARTESIAN_POINT('Origin',(8.08877866266397,-0.1,19.7283489784518));
#21221=CARTESIAN_POINT('',(7.88877866266397,-0.8,19.7283489784518));
#21222=CARTESIAN_POINT('Origin',(8.08877866266397,-0.1,19.7283489784518));
#23541=UNCERTAINTY_MEASURE_WITH_UNIT(LENGTH_MEASURE(0.001),#23729,
'DISTANCE_ACCURACY_VALUE',
'Maximum model space distance between geometric entities at asserted c
onnectivities');
#23611=UNCERTAINTY_MEASURE_WITH_UNIT(LENGTH_MEASURE(0.001),#23729,
'DISTANCE_ACCURACY_VALUE',
'Maximum model space distance between geometric entities at asserted c
onnectivities');
#23658=(
GEOMETRIC_REPRESENTATION_CONTEXT(3)
GLOBAL_UNCERTAINTY_ASSIGNED_CONTEXT((#23541))
GLOBAL_UNIT_ASSIGNED_CONTEXT((#23729,#23731,#23732))
REPRESENTATION_CONTEXT('','3D')
);
#23728=(
GEOMETRIC_REPRESENTATION_CONTEXT(3)
GLOBAL_UNCERTAINTY_ASSIGNED_CONTEXT((#23611))
GLOBAL_UNIT_ASSIGNED_CONTEXT((#23729,#23731,#23732))
REPRESENTATION_CONTEXT('','3D')
);
#23729=(
LENGTH_UNIT()
NAMED_UNIT(*)
SI_UNIT(.CENTI.,.METRE.)
);
#23731=(
NAMED_UNIT(*)
PLANE_ANGLE_UNIT()
SI_UNIT($,.RADIAN.)
);
#23732=(
NAMED_UNIT(*)
SI_UNIT($,.STERADIAN.)
SOLID_ANGLE_UNIT()
);
#23779=SHAPE_DEFINITION_REPRESENTATION(#23895,#24158);
#23895=PRODUCT_DEFINITION_SHAPE('',$,#24275);
#24158=SHAPE_REPRESENTATION('',(#14396),#23658);
#24228=PRODUCT_DEFINITION_CONTEXT('part definition',#24578,'design');
#24275=PRODUCT_DEFINITION('M4 short cap screw (9)',
'M4 short cap screw (9)',#24391,#24228);
#24391=PRODUCT_DEFINITION_FORMATION('',$,#24626);
#24578=APPLICATION_CONTEXT(
'Core Data for Automotive Mechanical Design Process');
#24579=PRODUCT_CONTEXT('part definition',#24578,'mechanical');
#24626=PRODUCT('M4 short cap screw (9)','M4 short cap screw (9)',
'M4 short cap screw (9)',(#24579));
#24766=COLOUR_RGB('Black',0.12,0.14,0.17);
#24767=FILL_AREA_STYLE_COLOUR('',#24766);
#24768=FILL_AREA_STYLE('',(#24767));
#24769=SURFACE_STYLE_FILL_AREA(#24768);
#24770=SURFACE_SIDE_STYLE('',(#24769));
#24771=SURFACE_STYLE_USAGE(.BOTH.,#24770);
#24772=PRESENTATION_STYLE_ASSIGNMENT((#24771));
ENDSEC;
END-ISO-10303-21;
